ISO-10303-21;
HEADER;
/* Generated by software containing ST-Developer
 * from STEP Tools, Inc. (www.steptools.com) 
 */

FILE_DESCRIPTION(
/* description */ ('Belt tension measurement rig'),
/* implementation_level */ '2;1');

FILE_NAME(
/* name */ 'Output M3 set screw (1).step',
/* time_stamp */ '2026-10-28T03:24:44-07:00',
/* author */ (''),
/* organization */ (''),
/* preprocessor_version */ 'ST-DEVELOPER v20.2',
/* originating_system */ 'Autodesk Translation Framework v15.17.0.0',
/* authorisation */ '');

FILE_SCHEMA (('AUTOMOTIVE_DESIGN { 1 0 10303 214 3 1 1 }'));
ENDSEC;

DATA;
#10=MECHANICAL_DESIGN_GEOMETRIC_PRESENTATION_REPRESENTATION('',(#755),#23587);
#630=SHAPE_REPRESENTATION_RELATIONSHIP('SRR','None',#23881,#685);
#685=ADVANCED_BREP_SHAPE_REPRESENTATION('',(#823),#23579);
#755=STYLED_ITEM('',(#24218),#823);
#823=MANIFOLD_SOLID_BREP('Body1',#12262);
#1310=PLANE('',#14060);
#1311=PLANE('',#14061);
#1903=FACE_OUTER_BOUND('',#2791,.T.);
#1904=FACE_OUTER_BOUND('',#2792,.T.);
#1905=FACE_OUTER_BOUND('',#2793,.T.);
#2791=EDGE_LOOP('',(#10378,#10379,#10380,#10381));
#2792=EDGE_LOOP('',(#10382));
#2793=EDGE_LOOP('',(#10383));
#3566=LINE('',#22226,#4317);
#4317=VECTOR('',#17481,0.15);
#5030=CIRCLE('',#14058,0.15);
#5031=CIRCLE('',#14059,0.15);
#6067=VERTEX_POINT('',#22223);
#6068=VERTEX_POINT('',#22225);
#7548=EDGE_CURVE('',#6067,#6067,#5030,.T.);
#7549=EDGE_CURVE('',#6067,#6068,#3566,.T.);
#7550=EDGE_CURVE('',#6068,#6068,#5031,.T.);
#10378=ORIENTED_EDGE('',*,*,#7548,.F.);
#10379=ORIENTED_EDGE('',*,*,#7549,.T.);
#10380=ORIENTED_EDGE('',*,*,#7550,.T.);
#10381=ORIENTED_EDGE('',*,*,#7549,.F.);
#10382=ORIENTED_EDGE('',*,*,#7548,.T.);
#10383=ORIENTED_EDGE('',*,*,#7550,.F.);
#11388=CYLINDRICAL_SURFACE('',#14057,0.15);
#12044=ADVANCED_FACE('',(#1903),#11388,.T.);
#12045=ADVANCED_FACE('',(#1904),#1310,.T.);
#12046=ADVANCED_FACE('',(#1905),#1311,.F.);
#12262=CLOSED_SHELL('',(#12044,#12045,#12046));
#14056=AXIS2_PLACEMENT_3D('',#22221,#17475,#17476);
#14057=AXIS2_PLACEMENT_3D('',#22222,#17477,#17478);
#14058=AXIS2_PLACEMENT_3D('',#22224,#17479,#17480);
#14059=AXIS2_PLACEMENT_3D('',#22227,#17482,#17483);
#14060=AXIS2_PLACEMENT_3D('',#22228,#17484,#17485);
#14061=AXIS2_PLACEMENT_3D('',#22229,#17486,#17487);
#17475=DIRECTION('axis',(0.,0.,1.));
#17476=DIRECTION('refdir',(1.,0.,0.));
#17477=DIRECTION('center_axis',(0.,0.,1.));
#17478=DIRECTION('ref_axis',(1.,0.,0.));
#17479=DIRECTION('center_axis',(0.,0.,1.));
#17480=DIRECTION('ref_axis',(1.,0.,0.));
#17481=DIRECTION('',(0.,0.,-1.));
#17482=DIRECTION('center_axis',(0.,0.,1.));
#17483=DIRECTION('ref_axis',(1.,0.,0.));
#17484=DIRECTION('center_axis',(0.,0.,1.));
#17485=DIRECTION('ref_axis',(1.,0.,0.));
#17486=DIRECTION('center_axis',(0.,0.,1.));
#17487=DIRECTION('ref_axis',(1.,0.,0.));
#22221=CARTESIAN_POINT('',(0.,0.,0.));
#22222=CARTESIAN_POINT('Origin',(10.,-4.,7.6));
#22223=CARTESIAN_POINT('',(9.85,-4.,8.));
#22224=CARTESIAN_POINT('Origin',(10.,-4.,8.));
#22225=CARTESIAN_POINT('',(9.85,-4.,7.6));
#22226=CARTESIAN_POINT('',(9.85,-4.,7.6));
#22227=CARTESIAN_POINT('Origin',(10.,-4.,7.6));
#22228=CARTESIAN_POINT('Origin',(10.,-4.,8.));
#22229=CARTESIAN_POINT('Origin',(10.,-4.,7.6));
#23514=UNCERTAINTY_MEASURE_WITH_UNIT(LENGTH_MEASURE(0.001),#23588,
'DISTANCE_ACCURACY_VALUE',
'Maximum model space distance between geometric entities at asserted c
onnectivities');
#23522=UNCERTAINTY_MEASURE_WITH_UNIT(LENGTH_MEASURE(0.001),#23588,
'DISTANCE_ACCURACY_VALUE',
'Maximum model space distance between geometric entities at asserted c
onnectivities');
#23579=(
GEOMETRIC_REPRESENTATION_CONTEXT(3)
GLOBAL_UNCERTAINTY_ASSIGNED_CONTEXT((#23514))
GLOBAL_UNIT_ASSIGNED_CONTEXT((#23588,#23590,#23591))
REPRESENTATION_CONTEXT('','3D')
);
#23587=(
GEOMETRIC_REPRESENTATION_CONTEXT(3)
GLOBAL_UNCERTAINTY_ASSIGNED_CONTEXT((#23522))
GLOBAL_UNIT_ASSIGNED_CONTEXT((#23588,#23590,#23591))
REPRESENTATION_CONTEXT('','3D')
);
#23588=(
LENGTH_UNIT()
NAMED_UNIT(*)
SI_UNIT(.CENTI.,.METRE.)
);
#23590=(
NAMED_UNIT(*)
PLANE_ANGLE_UNIT()
SI_UNIT($,.RADIAN.)
);
#23591=(
NAMED_UNIT(*)
SI_UNIT($,.STERADIAN.)
SOLID_ANGLE_UNIT()
);
#23648=SHAPE_DEFINITION_REPRESENTATION(#23725,#23881);
#23725=PRODUCT_DEFINITION_SHAPE('',$,#23946);
#23881=SHAPE_REPRESENTATION('',(#14056),#23579);
#23889=PRODUCT_DEFINITION_CONTEXT('part definition',#24083,'design');
#23946=PRODUCT_DEFINITION('Output M3 set screw (1)',
'Output M3 set screw (1)',#24010,#23889);
#24010=PRODUCT_DEFINITION_FORMATION('',$,#24141);
#24083=APPLICATION_CONTEXT(
'Core Data for Automotive Mechanical Design Process');
#24084=PRODUCT_CONTEXT('part definition',#24083,'mechanical');
#24141=PRODUCT('Output M3 set screw (1)','Output M3 set screw (1)',
'Output M3 set screw (1)',(#24084));
#24212=COLOUR_RGB('Black',0.12,0.14,0.17);
#24213=FILL_AREA_STYLE_COLOUR('',#24212);
#24214=FILL_AREA_STYLE('',(#24213));
#24215=SURFACE_STYLE_FILL_AREA(#24214);
#24216=SURFACE_SIDE_STYLE('',(#24215));
#24217=SURFACE_STYLE_USAGE(.BOTH.,#24216);
#24218=PRESENTATION_STYLE_ASSIGNMENT((#24217));
ENDSEC;
END-ISO-10303-21;
